ISO-10303-21;
HEADER;
/* Generated by software containing ST-Developer
 * from STEP Tools, Inc. (www.steptools.com) 
 */

FILE_DESCRIPTION(
/* description */ ('Line shaft on three pillow blocks'),
/* implementation_level */ '2;1');

FILE_NAME(
/* name */ 'Cap Screw - M5x20.step',
/* time_stamp */ '2026-10-27T10:49:19-07:00',
/* author */ (''),
/* organization */ (''),
/* preprocessor_version */ 'ST-DEVELOPER v20.2',
/* originating_system */ 'Autodesk Translation Framework v15.17.0.0',
/* authorisation */ '');

FILE_SCHEMA (('AUTOMOTIVE_DESIGN { 1 0 10303 214 3 1 1 }'));
ENDSEC;

DATA;
#10=MECHANICAL_DESIGN_GEOMETRIC_PRESENTATION_REPRESENTATION('',(#365),#8377);
#267=ORIENTED_CLOSED_SHELL('',*,#4354,.F.);
#277=CONICAL_SURFACE('',#5108,0.4,0.785398163397448);
#278=CONICAL_SURFACE('',#5112,0.41,0.785398163397448);
#279=CONICAL_SURFACE('',#5116,0.26,0.463647609000806);
#280=CONICAL_SURFACE('',#5120,0.225,0.785398163397448);
#283=BREP_WITH_VOIDS('Body1',#4353,(#267));
#310=SHAPE_REPRESENTATION_RELATIONSHIP('SRR','None',#8527,#337);
#337=ADVANCED_BREP_SHAPE_REPRESENTATION('',(#283),#8376);
#365=STYLED_ITEM('',(#8725),#283);
#487=FACE_BOUND('',#1242,.T.);
#643=PLANE('',#5106);
#644=PLANE('',#5114);
#645=PLANE('',#5122);
#646=PLANE('',#5123);
#647=PLANE('',#5124);
#648=PLANE('',#5125);
#649=PLANE('',#5126);
#650=PLANE('',#5127);
#651=PLANE('',#5128);
#652=PLANE('',#5129);
#653=PLANE('',#5130);
#889=FACE_OUTER_BOUND('',#1237,.T.);
#890=FACE_OUTER_BOUND('',#1238,.T.);
#891=FACE_OUTER_BOUND('',#1239,.T.);
#892=FACE_OUTER_BOUND('',#1240,.T.);
#893=FACE_OUTER_BOUND('',#1241,.T.);
#894=FACE_OUTER_BOUND('',#1243,.T.);
#895=FACE_OUTER_BOUND('',#1244,.T.);
#896=FACE_OUTER_BOUND('',#1245,.T.);
#897=FACE_OUTER_BOUND('',#1246,.T.);
#898=FACE_OUTER_BOUND('',#1247,.T.);
#899=FACE_OUTER_BOUND('',#1248,.T.);
#900=FACE_OUTER_BOUND('',#1249,.T.);
#901=FACE_OUTER_BOUND('',#1250,.T.);
#902=FACE_OUTER_BOUND('',#1251,.T.);
#903=FACE_OUTER_BOUND('',#1252,.T.);
#904=FACE_OUTER_BOUND('',#1253,.T.);
#905=FACE_OUTER_BOUND('',#1254,.T.);
#1237=EDGE_LOOP('',(#3937));
#1238=EDGE_LOOP('',(#3938,#3939,#3940,#3941));
#1239=EDGE_LOOP('',(#3942,#3943,#3944,#3945));
#1240=EDGE_LOOP('',(#3946,#3947,#3948,#3949));
#1241=EDGE_LOOP('',(#3950));
#1242=EDGE_LOOP('',(#3951));
#1243=EDGE_LOOP('',(#3952,#3953,#3954,#3955));
#1244=EDGE_LOOP('',(#3956,#3957,#3958,#3959));
#1245=EDGE_LOOP('',(#3960,#3961,#3962,#3963));
#1246=EDGE_LOOP('',(#3964));
#1247=EDGE_LOOP('',(#3965,#3966,#3967,#3968));
#1248=EDGE_LOOP('',(#3969,#3970,#3971,#3972));
#1249=EDGE_LOOP('',(#3973,#3974,#3975,#3976));
#1250=EDGE_LOOP('',(#3977,#3978,#3979,#3980));
#1251=EDGE_LOOP('',(#3981,#3982,#3983,#3984));
#1252=EDGE_LOOP('',(#3985,#3986,#3987,#3988));
#1253=EDGE_LOOP('',(#3989,#3990,#3991,#3992,#3993,#3994));
#1254=EDGE_LOOP('',(#3995,#3996,#3997,#3998,#3999,#4000));
#1558=LINE('',#8234,#1885);
#1559=LINE('',#8238,#1886);
#1560=LINE('',#8242,#1887);
#1561=LINE('',#8249,#1888);
#1562=LINE('',#8253,#1889);
#1563=LINE('',#8257,#1890);
#1564=LINE('',#8262,#1891);
#1565=LINE('',#8264,#1892);
#1566=LINE('',#8266,#1893);
#1567=LINE('',#8267,#1894);
#1568=LINE('',#8270,#1895);
#1569=LINE('',#8272,#1896);
#1570=LINE('',#8273,#1897);
#1571=LINE('',#8276,#1898);
#1572=LINE('',#8278,#1899);
#1573=LINE('',#8279,#1900);
#1574=LINE('',#8282,#1901);
#1575=LINE('',#8284,#1902);
#1576=LINE('',#8285,#1903);
#1577=LINE('',#8288,#1904);
#1578=LINE('',#8290,#1905);
#1579=LINE('',#8291,#1906);
#1580=LINE('',#8293,#1907);
#1581=LINE('',#8294,#1908);
#1885=VECTOR('',#6365,0.4);
#1886=VECTOR('',#6370,0.425);
#1887=VECTOR('',#6375,0.41);
#1888=VECTOR('',#6384,0.26);
#1889=VECTOR('',#6389,0.25);
#1890=VECTOR('',#6394,0.225);
#1891=VECTOR('',#6399,1.);
#1892=VECTOR('',#6400,1.);
#1893=VECTOR('',#6401,1.);
#1894=VECTOR('',#6402,1.);
#1895=VECTOR('',#6405,1.);
#1896=VECTOR('',#6406,1.);
#1897=VECTOR('',#6407,1.);
#1898=VECTOR('',#6410,1.);
#1899=VECTOR('',#6411,1.);
#1900=VECTOR('',#6412,1.);
#1901=VECTOR('',#6415,1.);
#1902=VECTOR('',#6416,1.);
#1903=VECTOR('',#6417,1.);
#1904=VECTOR('',#6420,1.);
#1905=VECTOR('',#6421,1.);
#1906=VECTOR('',#6422,1.);
#1907=VECTOR('',#6425,1.);
#1908=VECTOR('',#6426,1.);
#2060=CIRCLE('',#5107,0.375);
#2061=CIRCLE('',#5109,0.425);
#2062=CIRCLE('',#5111,0.425);
#2063=CIRCLE('',#5113,0.395);
#2064=CIRCLE('',#5115,0.27);
#2065=CIRCLE('',#5117,0.24505);
#2066=CIRCLE('',#5119,0.24505);
#2067=CIRCLE('',#5121,0.2);
#2403=VERTEX_POINT('',#8229);
#2404=VERTEX_POINT('',#8232);
#2405=VERTEX_POINT('',#8236);
#2406=VERTEX_POINT('',#8240);
#2407=VERTEX_POINT('',#8244);
#2408=VERTEX_POINT('',#8247);
#2409=VERTEX_POINT('',#8251);
#2410=VERTEX_POINT('',#8255);
#2411=VERTEX_POINT('',#8260);
#2412=VERTEX_POINT('',#8261);
#2413=VERTEX_POINT('',#8263);
#2414=VERTEX_POINT('',#8265);
#2415=VERTEX_POINT('',#8269);
#2416=VERTEX_POINT('',#8271);
#2417=VERTEX_POINT('',#8275);
#2418=VERTEX_POINT('',#8277);
#2419=VERTEX_POINT('',#8281);
#2420=VERTEX_POINT('',#8283);
#2421=VERTEX_POINT('',#8287);
#2422=VERTEX_POINT('',#8289);
#2917=EDGE_CURVE('',#2403,#2403,#2060,.T.);
#2918=EDGE_CURVE('',#2404,#2404,#2061,.T.);
#2919=EDGE_CURVE('',#2404,#2403,#1558,.T.);
#2920=EDGE_CURVE('',#2405,#2405,#2062,.T.);
#2921=EDGE_CURVE('',#2405,#2404,#1559,.T.);
#2922=EDGE_CURVE('',#2406,#2406,#2063,.T.);
#2923=EDGE_CURVE('',#2406,#2405,#1560,.T.);
#2924=EDGE_CURVE('',#2407,#2407,#2064,.T.);
#2925=EDGE_CURVE('',#2408,#2408,#2065,.F.);
#2926=EDGE_CURVE('',#2408,#2407,#1561,.T.);
#2927=EDGE_CURVE('',#2409,#2409,#2066,.F.);
#2928=EDGE_CURVE('',#2409,#2408,#1562,.T.);
#2929=EDGE_CURVE('',#2410,#2410,#2067,.T.);
#2930=EDGE_CURVE('',#2410,#2409,#1563,.T.);
#2931=EDGE_CURVE('',#2411,#2412,#1564,.T.);
#2932=EDGE_CURVE('',#2412,#2413,#1565,.T.);
#2933=EDGE_CURVE('',#2413,#2414,#1566,.T.);
#2934=EDGE_CURVE('',#2411,#2414,#1567,.T.);
#2935=EDGE_CURVE('',#2412,#2415,#1568,.T.);
#2936=EDGE_CURVE('',#2415,#2416,#1569,.T.);
#2937=EDGE_CURVE('',#2416,#2413,#1570,.T.);
#2938=EDGE_CURVE('',#2415,#2417,#1571,.T.);
#2939=EDGE_CURVE('',#2417,#2418,#1572,.T.);
#2940=EDGE_CURVE('',#2418,#2416,#1573,.T.);
#2941=EDGE_CURVE('',#2417,#2419,#1574,.T.);
#2942=EDGE_CURVE('',#2419,#2420,#1575,.T.);
#2943=EDGE_CURVE('',#2420,#2418,#1576,.T.);
#2944=EDGE_CURVE('',#2419,#2421,#1577,.T.);
#2945=EDGE_CURVE('',#2421,#2422,#1578,.T.);
#2946=EDGE_CURVE('',#2422,#2420,#1579,.T.);
#2947=EDGE_CURVE('',#2421,#2411,#1580,.T.);
#2948=EDGE_CURVE('',#2414,#2422,#1581,.T.);
#3937=ORIENTED_EDGE('',*,*,#2917,.F.);
#3938=ORIENTED_EDGE('',*,*,#2918,.F.);
#3939=ORIENTED_EDGE('',*,*,#2919,.T.);
#3940=ORIENTED_EDGE('',*,*,#2917,.T.);
#3941=ORIENTED_EDGE('',*,*,#2919,.F.);
#3942=ORIENTED_EDGE('',*,*,#2920,.F.);
#3943=ORIENTED_EDGE('',*,*,#2921,.T.);
#3944=ORIENTED_EDGE('',*,*,#2918,.T.);
#3945=ORIENTED_EDGE('',*,*,#2921,.F.);
#3946=ORIENTED_EDGE('',*,*,#2922,.F.);
#3947=ORIENTED_EDGE('',*,*,#2923,.T.);
#3948=ORIENTED_EDGE('',*,*,#2920,.T.);
#3949=ORIENTED_EDGE('',*,*,#2923,.F.);
#3950=ORIENTED_EDGE('',*,*,#2922,.T.);
#3951=ORIENTED_EDGE('',*,*,#2924,.F.);
#3952=ORIENTED_EDGE('',*,*,#2925,.F.);
#3953=ORIENTED_EDGE('',*,*,#2926,.T.);
#3954=ORIENTED_EDGE('',*,*,#2924,.T.);
#3955=ORIENTED_EDGE('',*,*,#2926,.F.);
#3956=ORIENTED_EDGE('',*,*,#2927,.F.);
#3957=ORIENTED_EDGE('',*,*,#2928,.T.);
#3958=ORIENTED_EDGE('',*,*,#2925,.T.);
#3959=ORIENTED_EDGE('',*,*,#2928,.F.);
#3960=ORIENTED_EDGE('',*,*,#2929,.F.);
#3961=ORIENTED_EDGE('',*,*,#2930,.T.);
#3962=ORIENTED_EDGE('',*,*,#2927,.T.);
#3963=ORIENTED_EDGE('',*,*,#2930,.F.);
#3964=ORIENTED_EDGE('',*,*,#2929,.T.);
#3965=ORIENTED_EDGE('',*,*,#2931,.T.);
#3966=ORIENTED_EDGE('',*,*,#2932,.T.);
#3967=ORIENTED_EDGE('',*,*,#2933,.T.);
#3968=ORIENTED_EDGE('',*,*,#2934,.F.);
#3969=ORIENTED_EDGE('',*,*,#2935,.T.);
#3970=ORIENTED_EDGE('',*,*,#2936,.T.);
#3971=ORIENTED_EDGE('',*,*,#2937,.T.);
#3972=ORIENTED_EDGE('',*,*,#2932,.F.);
#3973=ORIENTED_EDGE('',*,*,#2938,.T.);
#3974=ORIENTED_EDGE('',*,*,#2939,.T.);
#3975=ORIENTED_EDGE('',*,*,#2940,.T.);
#3976=ORIENTED_EDGE('',*,*,#2936,.F.);
#3977=ORIENTED_EDGE('',*,*,#2941,.T.);
#3978=ORIENTED_EDGE('',*,*,#2942,.T.);
#3979=ORIENTED_EDGE('',*,*,#2943,.T.);
#3980=ORIENTED_EDGE('',*,*,#2939,.F.);
#3981=ORIENTED_EDGE('',*,*,#2944,.T.);
#3982=ORIENTED_EDGE('',*,*,#2945,.T.);
#3983=ORIENTED_EDGE('',*,*,#2946,.T.);
#3984=ORIENTED_EDGE('',*,*,#2942,.F.);
#3985=ORIENTED_EDGE('',*,*,#2947,.T.);
#3986=ORIENTED_EDGE('',*,*,#2934,.T.);
#3987=ORIENTED_EDGE('',*,*,#2948,.T.);
#3988=ORIENTED_EDGE('',*,*,#2945,.F.);
#3989=ORIENTED_EDGE('',*,*,#2947,.F.);
#3990=ORIENTED_EDGE('',*,*,#2944,.F.);
#3991=ORIENTED_EDGE('',*,*,#2941,.F.);
#3992=ORIENTED_EDGE('',*,*,#2938,.F.);
#3993=ORIENTED_EDGE('',*,*,#2935,.F.);
#3994=ORIENTED_EDGE('',*,*,#2931,.F.);
#3995=ORIENTED_EDGE('',*,*,#2948,.F.);
#3996=ORIENTED_EDGE('',*,*,#2933,.F.);
#3997=ORIENTED_EDGE('',*,*,#2937,.F.);
#3998=ORIENTED_EDGE('',*,*,#2940,.F.);
#3999=ORIENTED_EDGE('',*,*,#2943,.F.);
#4000=ORIENTED_EDGE('',*,*,#2946,.F.);
#4070=CYLINDRICAL_SURFACE('',#5110,0.425);
#4071=CYLINDRICAL_SURFACE('',#5118,0.24505);
#4307=ADVANCED_FACE('',(#889),#643,.T.);
#4308=ADVANCED_FACE('',(#890),#277,.T.);
#4309=ADVANCED_FACE('',(#891),#4070,.T.);
#4310=ADVANCED_FACE('',(#892),#278,.T.);
#4311=ADVANCED_FACE('',(#893,#487),#644,.T.);
#4312=ADVANCED_FACE('',(#894),#279,.T.);
#4313=ADVANCED_FACE('',(#895),#4071,.T.);
#4314=ADVANCED_FACE('',(#896),#280,.T.);
#4315=ADVANCED_FACE('',(#897),#645,.T.);
#4316=ADVANCED_FACE('',(#898),#646,.F.);
#4317=ADVANCED_FACE('',(#899),#647,.F.);
#4318=ADVANCED_FACE('',(#900),#648,.F.);
#4319=ADVANCED_FACE('',(#901),#649,.F.);
#4320=ADVANCED_FACE('',(#902),#650,.F.);
#4321=ADVANCED_FACE('',(#903),#651,.F.);
#4322=ADVANCED_FACE('',(#904),#652,.F.);
#4323=ADVANCED_FACE('',(#905),#653,.F.);
#4353=CLOSED_SHELL('',(#4307,#4308,#4309,#4310,#4311,#4312,#4313,#4314,
#4315));
#4354=CLOSED_SHELL('',(#4316,#4317,#4318,#4319,#4320,#4321,#4322,#4323));
#5105=AXIS2_PLACEMENT_3D('',#8227,#6355,#6356);
#5106=AXIS2_PLACEMENT_3D('',#8228,#6357,#6358);
#5107=AXIS2_PLACEMENT_3D('',#8230,#6359,#6360);
#5108=AXIS2_PLACEMENT_3D('',#8231,#6361,#6362);
#5109=AXIS2_PLACEMENT_3D('',#8233,#6363,#6364);
#5110=AXIS2_PLACEMENT_3D('',#8235,#6366,#6367);
#5111=AXIS2_PLACEMENT_3D('',#8237,#6368,#6369);
#5112=AXIS2_PLACEMENT_3D('',#8239,#6371,#6372);
#5113=AXIS2_PLACEMENT_3D('',#8241,#6373,#6374);
#5114=AXIS2_PLACEMENT_3D('',#8243,#6376,#6377);
#5115=AXIS2_PLACEMENT_3D('',#8245,#6378,#6379);
#5116=AXIS2_PLACEMENT_3D('',#8246,#6380,#6381);
#5117=AXIS2_PLACEMENT_3D('',#8248,#6382,#6383);
#5118=AXIS2_PLACEMENT_3D('',#8250,#6385,#6386);
#5119=AXIS2_PLACEMENT_3D('',#8252,#6387,#6388);
#5120=AXIS2_PLACEMENT_3D('',#8254,#6390,#6391);
#5121=AXIS2_PLACEMENT_3D('',#8256,#6392,#6393);
#5122=AXIS2_PLACEMENT_3D('',#8258,#6395,#6396);
#5123=AXIS2_PLACEMENT_3D('',#8259,#6397,#6398);
#5124=AXIS2_PLACEMENT_3D('',#8268,#6403,#6404);
#5125=AXIS2_PLACEMENT_3D('',#8274,#6408,#6409);
#5126=AXIS2_PLACEMENT_3D('',#8280,#6413,#6414);
#5127=AXIS2_PLACEMENT_3D('',#8286,#6418,#6419);
#5128=AXIS2_PLACEMENT_3D('',#8292,#6423,#6424);
#5129=AXIS2_PLACEMENT_3D('',#8295,#6427,#6428);
#5130=AXIS2_PLACEMENT_3D('',#8296,#6429,#6430);
#6355=DIRECTION('axis',(0.,0.,1.));
#6356=DIRECTION('refdir',(1.,0.,0.));
#6357=DIRECTION('center_axis',(0.,1.,0.));
#6358=DIRECTION('ref_axis',(0.,0.,1.));
#6359=DIRECTION('center_axis',(0.,-1.,0.));
#6360=DIRECTION('ref_axis',(1.,0.,0.));
#6361=DIRECTION('center_axis',(0.,-1.,0.));
#6362=DIRECTION('ref_axis',(1.,0.,0.));
#6363=DIRECTION('center_axis',(0.,-1.,0.));
#6364=DIRECTION('ref_axis',(1.,0.,0.));
#6365=DIRECTION('',(0.707106781186548,0.707106781186547,8.65956056235493E-17));
#6366=DIRECTION('center_axis',(0.,-1.,0.));
#6367=DIRECTION('ref_axis',(1.,0.,0.));
#6368=DIRECTION('center_axis',(0.,-1.,0.));
#6369=DIRECTION('ref_axis',(1.,0.,0.));
#6370=DIRECTION('',(0.,1.,0.));
#6371=DIRECTION('center_axis',(0.,1.,0.));
#6372=DIRECTION('ref_axis',(1.,0.,0.));
#6373=DIRECTION('center_axis',(0.,-1.,0.));
#6374=DIRECTION('ref_axis',(1.,0.,0.));
#6375=DIRECTION('',(-0.707106781186547,0.707106781186548,-8.65956056235493E-17));
#6376=DIRECTION('center_axis',(0.,-1.,0.));
#6377=DIRECTION('ref_axis',(0.,0.,-1.));
#6378=DIRECTION('center_axis',(0.,-1.,0.));
#6379=DIRECTION('ref_axis',(1.,0.,0.));
#6380=DIRECTION('center_axis',(0.,1.,0.));
#6381=DIRECTION('ref_axis',(1.,0.,0.));
#6382=DIRECTION('center_axis',(0.,1.,0.));
#6383=DIRECTION('ref_axis',(1.,0.,0.));
#6384=DIRECTION('',(-0.447213595499958,0.894427190999916,-5.47678698264203E-17));
#6385=DIRECTION('center_axis',(0.,-1.,0.));
#6386=DIRECTION('ref_axis',(1.,0.,0.));
#6387=DIRECTION('center_axis',(0.,1.,0.));
#6388=DIRECTION('ref_axis',(1.,0.,0.));
#6389=DIRECTION('',(0.,1.,0.));
#6390=DIRECTION('center_axis',(0.,1.,0.));
#6391=DIRECTION('ref_axis',(1.,0.,0.));
#6392=DIRECTION('center_axis',(0.,-1.,0.));
#6393=DIRECTION('ref_axis',(1.,0.,0.));
#6394=DIRECTION('',(-0.707106781186547,0.707106781186548,-8.65956056235493E-17));
#6395=DIRECTION('center_axis',(0.,-1.,0.));
#6396=DIRECTION('ref_axis',(0.,0.,-1.));
#6397=DIRECTION('center_axis',(0.866025403784439,0.,-0.5));
#6398=DIRECTION('ref_axis',(0.5,0.,0.866025403784439));
#6399=DIRECTION('',(-0.5,0.,-0.866025403784439));
#6400=DIRECTION('',(0.,-1.,0.));
#6401=DIRECTION('',(0.5,0.,0.866025403784439));
#6402=DIRECTION('',(0.,-1.,0.));
#6403=DIRECTION('center_axis',(1.20185167898973E-16,0.,-1.));
#6404=DIRECTION('ref_axis',(1.,0.,1.20185167898973E-16));
#6405=DIRECTION('',(-1.,0.,-1.20185167898973E-16));
#6406=DIRECTION('',(0.,-1.,0.));
#6407=DIRECTION('',(1.,0.,1.20185167898973E-16));
#6408=DIRECTION('center_axis',(-0.866025403784439,0.,-0.5));
#6409=DIRECTION('ref_axis',(0.5,0.,-0.866025403784439));
#6410=DIRECTION('',(-0.5,0.,0.866025403784439));
#6411=DIRECTION('',(0.,-1.,0.));
#6412=DIRECTION('',(0.5,0.,-0.866025403784439));
#6413=DIRECTION('center_axis',(-0.866025403784439,0.,0.5));
#6414=DIRECTION('ref_axis',(-0.5,0.,-0.866025403784439));
#6415=DIRECTION('',(0.5,0.,0.866025403784439));
#6416=DIRECTION('',(0.,-1.,0.));
#6417=DIRECTION('',(-0.5,0.,-0.866025403784439));
#6418=DIRECTION('center_axis',(-2.40370335797945E-16,0.,1.));
#6419=DIRECTION('ref_axis',(-1.,0.,-2.40370335797945E-16));
#6420=DIRECTION('',(1.,0.,2.40370335797945E-16));
#6421=DIRECTION('',(0.,-1.,0.));
#6422=DIRECTION('',(-1.,0.,-2.40370335797945E-16));
#6423=DIRECTION('center_axis',(0.866025403784439,0.,0.5));
#6424=DIRECTION('ref_axis',(-0.5,0.,0.866025403784439));
#6425=DIRECTION('',(0.5,0.,-0.866025403784439));
#6426=DIRECTION('',(-0.5,0.,0.866025403784439));
#6427=DIRECTION('center_axis',(0.,1.,0.));
#6428=DIRECTION('ref_axis',(1.,0.,0.));
#6429=DIRECTION('center_axis',(0.,-1.,0.));
#6430=DIRECTION('ref_axis',(0.,0.,-1.));
#8227=CARTESIAN_POINT('',(0.,0.,0.));
#8228=CARTESIAN_POINT('Origin',(0.375,0.5,0.));
#8229=CARTESIAN_POINT('',(-0.375,0.5,-4.59242549680257E-17));
#8230=CARTESIAN_POINT('Origin',(0.,0.5,0.));
#8231=CARTESIAN_POINT('Origin',(0.,0.475,0.));
#8232=CARTESIAN_POINT('',(-0.425,0.45,-5.20474889637625E-17));
#8233=CARTESIAN_POINT('Origin',(0.,0.45,0.));
#8234=CARTESIAN_POINT('',(-0.4,0.475,-4.89858719658941E-17));
#8235=CARTESIAN_POINT('Origin',(0.,0.24,0.));
#8236=CARTESIAN_POINT('',(-0.425,0.0299999999999998,-5.20474889637625E-17));
#8237=CARTESIAN_POINT('Origin',(0.,0.0299999999999998,0.));
#8238=CARTESIAN_POINT('',(-0.425,0.24,-5.20474889637625E-17));
#8239=CARTESIAN_POINT('Origin',(0.,0.0150000000000001,0.));
#8240=CARTESIAN_POINT('',(-0.395,4.85722573273506E-17,-4.83735485663204E-17));
#8241=CARTESIAN_POINT('Origin',(0.,0.,0.));
#8242=CARTESIAN_POINT('',(-0.41,0.0150000000000001,-5.02105187650415E-17));
#8243=CARTESIAN_POINT('Origin',(0.27,0.,0.));
#8244=CARTESIAN_POINT('',(-0.27,0.,-3.30654635769785E-17));
#8245=CARTESIAN_POINT('Origin',(0.,0.,0.));
#8246=CARTESIAN_POINT('Origin',(0.,-0.02,0.));
#8247=CARTESIAN_POINT('',(-0.24505,-0.0498999999999999,3.00099698131059E-17));
#8248=CARTESIAN_POINT('Origin',(0.,-0.0498999999999999,0.));
#8249=CARTESIAN_POINT('',(-0.26,-0.02,-3.18408167778312E-17));
#8250=CARTESIAN_POINT('Origin',(0.,-0.995,0.));
#8251=CARTESIAN_POINT('',(-0.24505,-1.95495,3.00099698131059E-17));
#8252=CARTESIAN_POINT('Origin',(0.,-1.95495,0.));
#8253=CARTESIAN_POINT('',(-0.24505,-0.995,-3.00099698131059E-17));
#8254=CARTESIAN_POINT('Origin',(0.,-1.975,0.));
#8255=CARTESIAN_POINT('',(-0.2,-2.,-2.44929359829471E-17));
#8256=CARTESIAN_POINT('Origin',(0.,-2.,0.));
#8257=CARTESIAN_POINT('',(-0.225,-1.975,-2.75545529808154E-17));
#8258=CARTESIAN_POINT('Origin',(0.,-2.,0.));
#8259=CARTESIAN_POINT('Origin',(0.115470053837925,-0.5,-0.2));
#8260=CARTESIAN_POINT('',(0.23094010767585,-0.5,0.));
#8261=CARTESIAN_POINT('',(0.115470053837925,-0.5,-0.2));
#8262=CARTESIAN_POINT('',(0.23094010767585,-0.5,0.));
#8263=CARTESIAN_POINT('',(0.115470053837925,-0.8,-0.2));
#8264=CARTESIAN_POINT('',(0.115470053837925,-0.5,-0.2));
#8265=CARTESIAN_POINT('',(0.23094010767585,-0.8,0.));
#8266=CARTESIAN_POINT('',(0.23094010767585,-0.8,0.));
#8267=CARTESIAN_POINT('',(0.23094010767585,-0.5,0.));
#8268=CARTESIAN_POINT('Origin',(-0.115470053837925,-0.5,-0.2));
#8269=CARTESIAN_POINT('',(-0.115470053837925,-0.5,-0.2));
#8270=CARTESIAN_POINT('',(0.115470053837925,-0.5,-0.2));
#8271=CARTESIAN_POINT('',(-0.115470053837925,-0.8,-0.2));
#8272=CARTESIAN_POINT('',(-0.115470053837925,-0.5,-0.2));
#8273=CARTESIAN_POINT('',(0.115470053837925,-0.8,-0.2));
#8274=CARTESIAN_POINT('Origin',(-0.23094010767585,-0.5,-2.77555756156289E-17));
#8275=CARTESIAN_POINT('',(-0.23094010767585,-0.5,-2.82820063659975E-17));
#8276=CARTESIAN_POINT('',(-0.115470053837925,-0.5,-0.2));
#8277=CARTESIAN_POINT('',(-0.23094010767585,-0.8,-2.77555756156289E-17));
#8278=CARTESIAN_POINT('',(-0.23094010767585,-0.5,-2.82820063659975E-17));
#8279=CARTESIAN_POINT('',(-0.115470053837925,-0.8,-0.2));
#8280=CARTESIAN_POINT('Origin',(-0.115470053837925,-0.5,0.2));
#8281=CARTESIAN_POINT('',(-0.115470053837925,-0.5,0.2));
#8282=CARTESIAN_POINT('',(-0.23094010767585,-0.5,-2.82820063659975E-17));
#8283=CARTESIAN_POINT('',(-0.115470053837925,-0.8,0.2));
#8284=CARTESIAN_POINT('',(-0.115470053837925,-0.5,0.2));
#8285=CARTESIAN_POINT('',(-0.23094010767585,-0.8,-2.82820063659975E-17));
#8286=CARTESIAN_POINT('Origin',(0.115470053837925,-0.5,0.2));
#8287=CARTESIAN_POINT('',(0.115470053837925,-0.5,0.2));
#8288=CARTESIAN_POINT('',(-0.115470053837925,-0.5,0.2));
#8289=CARTESIAN_POINT('',(0.115470053837925,-0.8,0.2));
#8290=CARTESIAN_POINT('',(0.115470053837925,-0.5,0.2));
#8291=CARTESIAN_POINT('',(-0.115470053837925,-0.8,0.2));
#8292=CARTESIAN_POINT('Origin',(0.23094010767585,-0.5,0.));
#8293=CARTESIAN_POINT('',(0.115470053837925,-0.5,0.2));
#8294=CARTESIAN_POINT('',(0.115470053837925,-0.8,0.2));
#8295=CARTESIAN_POINT('Origin',(0.,-0.5,0.));
#8296=CARTESIAN_POINT('Origin',(0.,-0.8,0.));
#8344=UNCERTAINTY_MEASURE_WITH_UNIT(LENGTH_MEASURE(0.001),#8378,
'DISTANCE_ACCURACY_VALUE',
'Maximum model space distance between geometric entities at asserted c
onnectivities');
#8345=UNCERTAINTY_MEASURE_WITH_UNIT(LENGTH_MEASURE(0.001),#8378,
'DISTANCE_ACCURACY_VALUE',
'Maximum model space distance between geometric entities at asserted c
onnectivities');
#8376=(
GEOMETRIC_REPRESENTATION_CONTEXT(3)
GLOBAL_UNCERTAINTY_ASSIGNED_CONTEXT((#8344))
GLOBAL_UNIT_ASSIGNED_CONTEXT((#8378,#8380,#8381))
REPRESENTATION_CONTEXT('','3D')
);
#8377=(
GEOMETRIC_REPRESENTATION_CONTEXT(3)
GLOBAL_UNCERTAINTY_ASSIGNED_CONTEXT((#8345))
GLOBAL_UNIT_ASSIGNED_CONTEXT((#8378,#8380,#8381))
REPRESENTATION_CONTEXT('','3D')
);
#8378=(
LENGTH_UNIT()
NAMED_UNIT(*)
SI_UNIT(.CENTI.,.METRE.)
);
#8380=(
NAMED_UNIT(*)
PLANE_ANGLE_UNIT()
SI_UNIT($,.RADIAN.)
);
#8381=(
NAMED_UNIT(*)
SI_UNIT($,.STERADIAN.)
SOLID_ANGLE_UNIT()
);
#8412=SHAPE_DEFINITION_REPRESENTATION(#8479,#8527);
#8479=PRODUCT_DEFINITION_SHAPE('',$,#8559);
#8527=SHAPE_REPRESENTATION('',(#5105),#8376);
#8528=PRODUCT_DEFINITION_CONTEXT('part definition',#8623,'design');
#8559=PRODUCT_DEFINITION('Cap Screw - M5x20','Cap Screw - M5x20',#8590,
#8528);
#8590=PRODUCT_DEFINITION_FORMATION('',$,#8655);
#8623=APPLICATION_CONTEXT(
'Core Data for Automotive Mechanical Design Process');
#8624=PRODUCT_CONTEXT('part definition',#8623,'mechanical');
#8655=PRODUCT('Cap Screw - M5x20','Cap Screw - M5x20',
'Cap Screw - M5x20',(#8624));
#8719=COLOUR_RGB('Black',0.12,0.14,0.17);
#8720=FILL_AREA_STYLE_COLOUR('',#8719);
#8721=FILL_AREA_STYLE('',(#8720));
#8722=SURFACE_STYLE_FILL_AREA(#8721);
#8723=SURFACE_SIDE_STYLE('',(#8722));
#8724=SURFACE_STYLE_USAGE(.BOTH.,#8723);
#8725=PRESENTATION_STYLE_ASSIGNMENT((#8724));
ENDSEC;
END-ISO-10303-21;
